ISO-10303-21;
HEADER;
FILE_DESCRIPTION (('STEP AP214'),
    '1' );
FILE_NAME ('socket head cap screw_iso_ISO 4762 M5 x 20 - 20N.step',
    '2026-10-24T13:33:06',
    ( '' ),
    ( '' ),
    'SwSTEP 2.0',
    'SolidWorks 2026',
    '' );
FILE_SCHEMA (( 'AUTOMOTIVE_DESIGN' ));
ENDSEC;

DATA;
#7=EDGE_LOOP ( 'NONE', ( #4823, #10214, #8474, #13193, #10057 ) ) ;
#33=DIRECTION ( 'NONE',  ( -1.000000000000000000, -0.000000000000000000, -0.000000000000000000 ) ) ;
#42=FACE_OUTER_BOUND ( 'NONE', #11021, .T. ) ;
#63=CARTESIAN_POINT ( 'NONE',  ( 2.500000000000000000, 0.000000000000000000, 0.000000000000000000 ) ) ;
#80=EDGE_LOOP ( 'NONE', ( #13793, #10829, #6578 ) ) ;
#105=CARTESIAN_POINT ( 'NONE',  ( 5.000000000000000888, 0.000000000000000000, 0.000000000000000000 ) ) ;
#133=DIRECTION ( 'NONE',  ( 1.000000000000000000, 0.000000000000000000, 0.000000000000000000 ) ) ;
#148=CIRCLE ( 'NONE', #8278, 4.000000000000000000 ) ;
#165=CARTESIAN_POINT ( 'NONE',  ( 5.000000000000000888, 4.250000000000000000, 0.000000000000000000 ) ) ;
#179=ORIENTED_EDGE ( 'NONE', *, *, #5778, .F. ) ;
#182=CARTESIAN_POINT ( 'NONE',  ( 2.500000000000000000, -1.768423874527823791, -1.020999999999998353 ) ) ;
#203=DIRECTION ( 'NONE',  ( 0.000000000000000000, 0.000000000000000000, 1.000000000000000000 ) ) ;
#212=VECTOR ( 'NONE', #10286, 1000.000000000000114 ) ;
#230=LINE ( 'NONE', #296, #13478 ) ;
#236=DIRECTION ( 'NONE',  ( 1.000000000000000000, 0.000000000000000000, 0.000000000000000000 ) ) ;
#263=EDGE_CURVE ( 'NONE', #5128, #8193, #4654, .T. ) ;
#296=CARTESIAN_POINT ( 'NONE',  ( 2.500000000000000000, 1.178949249685218525, 2.041999999999999371 ) ) ;
#337=PRESENTATION_STYLE_ASSIGNMENT (( #2631 ) ) ;
#344=EDGE_CURVE ( 'NONE', #3380, #915, #1258, .T. ) ;
#351=DIRECTION ( 'NONE',  ( -1.000000000000000000, -0.000000000000000000, -0.000000000000000000 ) ) ;
#404=CIRCLE ( 'NONE', #11796, 0.2000000000000000944 ) ;
#411=FILL_AREA_STYLE_COLOUR ( '', #13957 ) ;
#414=PRODUCT_CONTEXT ( 'NONE', #12033, 'mechanical' ) ;
#415=FACE_OUTER_BOUND ( 'NONE', #2522, .T. ) ;
#423=DIRECTION ( 'NONE',  ( -0.7071067811865306973, 8.659560562355138702E-17, -0.7071067811865643371 ) ) ;
#433=CARTESIAN_POINT ( 'NONE',  ( 0.000000000000000000, 2.357898499370433054, -1.951563910473907981E-15 ) ) ;
#451=PLANE ( 'NONE',  #2762 ) ;
#457=DIRECTION ( 'NONE',  ( 0.000000000000000000, 0.000000000000000000, -1.000000000000000000 ) ) ;
#461=CARTESIAN_POINT ( 'NONE',  ( 2.500000000000000000, -2.357898499370432610, 3.252606517456513302E-15 ) ) ;
#462=( GEOMETRIC_REPRESENTATION_CONTEXT ( 3 ) GLOBAL_UNCERTAINTY_ASSIGNED_CONTEXT ( ( #11763 ) ) GLOBAL_UNIT_ASSIGNED_CONTEXT ( ( #13639, #8054, #9372 ) ) REPRESENTATION_CONTEXT ( 'NONE', 'WORKASPACE' ) );
#556=DIRECTION ( 'NONE',  ( 1.000000000000000000, 0.000000000000000000, 0.000000000000000000 ) ) ;
#562=DIRECTION ( 'NONE',  ( 0.000000000000000000, 0.000000000000000000, 1.000000000000000000 ) ) ;
#618=ADVANCED_FACE ( 'NONE', ( #13049 ), #6593, .T. ) ;
#619=CARTESIAN_POINT ( 'NONE',  ( 2.500000000000000000, 1.768423874527824902, 1.020999999999999019 ) ) ;
#631=LINE ( 'NONE', #3992, #11133 ) ;
#632=ORIENTED_EDGE ( 'NONE', *, *, #9818, .T. ) ;
#645=DIRECTION ( 'NONE',  ( 0.000000000000000000, 0.000000000000000000, 1.000000000000000000 ) ) ;
#651=AXIS2_PLACEMENT_3D ( 'NONE', #4786, #10439, #3836 ) ;
#681=DIRECTION ( 'NONE',  ( 0.000000000000000000, 0.000000000000000000, -1.000000000000000000 ) ) ;
#695=AXIS2_PLACEMENT_3D ( 'NONE', #1037, #5488, #9920 ) ;
#698=DIRECTION ( 'NONE',  ( -1.000000000000000000, -0.000000000000000000, -0.000000000000000000 ) ) ;
#705=EDGE_CURVE ( 'NONE', #8299, #11820, #1204, .T. ) ;
#710=AXIS2_PLACEMENT_3D ( 'NONE', #12147, #4322, #3386 ) ;
#722=VERTEX_POINT ( 'NONE', #12315 ) ;
#731=( GEOMETRIC_REPRESENTATION_CONTEXT ( 3 ) GLOBAL_UNCERTAINTY_ASSIGNED_CONTEXT ( ( #3078 ) ) GLOBAL_UNIT_ASSIGNED_CONTEXT ( ( #5611, #5743, #3573 ) ) REPRESENTATION_CONTEXT ( 'NONE', 'WORKASPACE' ) );
#753=FACE_OUTER_BOUND ( 'NONE', #6198, .T. ) ;
#755=ORIENTED_EDGE ( 'NONE', *, *, #8686, .T. ) ;
#803=DIRECTION ( 'NONE',  ( -0.000000000000000000, 1.000000000000000000, 1.224646799147353207E-16 ) ) ;
#825=EDGE_CURVE ( 'NONE', #915, #3380, #3940, .T. ) ;
#827=CIRCLE ( 'NONE', #9659, 2.700000000000001066 ) ;
#838=AXIS2_PLACEMENT_3D ( 'NONE', #5898, #351, #4822 ) ;
#907=CARTESIAN_POINT ( 'NONE',  ( 2.500000000000000000, 0.000000000000000000, 0.000000000000000000 ) ) ;
#915=VERTEX_POINT ( 'NONE', #10650 ) ;
#939=CARTESIAN_POINT ( 'NONE',  ( 5.000000000000002665, 3.306546357697854226E-16, 2.700000000000001066 ) ) ;
#966=ADVANCED_FACE ( 'NONE', ( #8168 ), #7080, .T. ) ;
#980=EDGE_CURVE ( 'NONE', #3164, #7302, #13034, .T. ) ;
#1007=EDGE_CURVE ( 'NONE', #8136, #2366, #3112, .T. ) ;
#1014=FACE_OUTER_BOUND ( 'NONE', #10764, .T. ) ;
#1017=CARTESIAN_POINT ( 'NONE',  ( 2.500000000000000000, 1.178949249685213863, -2.042000000000001148 ) ) ;
#1030=ADVANCED_FACE ( 'NONE', ( #753 ), #7415, .T. ) ;
#1032=CARTESIAN_POINT ( 'NONE',  ( 2.500000000000000000, -1.178949249685218303, -2.041999999999998039 ) ) ;
#1037=CARTESIAN_POINT ( 'NONE',  ( 25.00000000000000000, 0.000000000000000000, 0.000000000000000000 ) ) ;
#1047=AXIS2_PLACEMENT_3D ( 'NONE', #6540, #14218, #10826 ) ;
#1061=DIRECTION ( 'NONE',  ( 0.000000000000000000, 0.5000000000000012212, 0.8660254037844380415 ) ) ;
#1082=DIRECTION ( 'NONE',  ( 1.000000000000000000, 0.000000000000000000, 0.000000000000000000 ) ) ;
#1119=CARTESIAN_POINT ( 'NONE',  ( 0.000000000000000000, 5.051668046482832750E-16, -4.000000000000000000 ) ) ;
#1127=VERTEX_POINT ( 'NONE', #2492 ) ;
#1136=AXIS2_PLACEMENT_3D ( 'NONE', #13097, #6510, #14116 ) ;
#1162=EDGE_CURVE ( 'NONE', #1127, #2687, #4887, .T. ) ;
#1185=LINE ( 'NONE', #5687, #3265 ) ;
#1197=PLANE ( 'NONE',  #14279 ) ;
#1198=AXIS2_PLACEMENT_3D ( 'NONE', #10088, #4870, #4583 ) ;
#1204=LINE ( 'NONE', #12460, #4769 ) ;
#1242=ORIENTED_EDGE ( 'NONE', *, *, #13470, .F. ) ;
#1258=CIRCLE ( 'NONE', #12860, 2.500000000000001332 ) ;
#1265=FACE_BOUND ( 'NONE', #12172, .T. ) ;
#1278=FACE_OUTER_BOUND ( 'NONE', #13437, .T. ) ;
#1304=CARTESIAN_POINT ( 'NONE',  ( 2.500000000000000000, -1.178949249685213863, 2.042000000000002924 ) ) ;
#1378=CARTESIAN_POINT ( 'NONE',  ( 5.200000000000002842, 0.000000000000000000, 2.500000000000000888 ) ) ;
#1398=CARTESIAN_POINT ( 'NONE',  ( 0.000000000000000000, -1.178949249685218303, -2.041999999999998039 ) ) ;
#1400=VERTEX_POINT ( 'NONE', #13069 ) ;
#1409=DIRECTION ( 'NONE',  ( 0.000000000000000000, 0.000000000000000000, -1.000000000000000000 ) ) ;
#1425=ADVANCED_BREP_SHAPE_REPRESENTATION ( '', ( #3853, #14039 ), #731 ) ;
#1450=DIRECTION ( 'NONE',  ( 0.000000000000000000, 0.000000000000000000, 1.000000000000000000 ) ) ;
#1492=CYLINDRICAL_SURFACE ( 'NONE', #2708, 4.250000000000000000 ) ;
#1497=CARTESIAN_POINT ( 'NONE',  ( 2.500000000000000000, 2.357898499370433054, -1.951563910473907981E-15 ) ) ;
#1526=ORIENTED_EDGE ( 'NONE', *, *, #263, .T. ) ;
#1528=DIRECTION ( 'NONE',  ( 0.000000000000000000, 0.000000000000000000, -1.000000000000000000 ) ) ;
#1529=AXIS2_PLACEMENT_3D ( 'NONE', #2301, #4549, #6656 ) ;
#1535=ADVANCED_FACE ( 'NONE', ( #6964 ), #10723, .T. ) ;
#1604=LINE ( 'NONE', #5975, #7116 ) ;
#1609=EDGE_CURVE ( 'NONE', #8612, #3475, #7899, .T. ) ;
#1694=EDGE_CURVE ( 'NONE', #4527, #2366, #7834, .T. ) ;
#1700=DIRECTION ( 'NONE',  ( 0.000000000000000000, 0.4999999999999993339, -0.8660254037844390407 ) ) ;
#1758=EDGE_LOOP ( 'NONE', ( #2832, #4777, #13936 ) ) ;
#1775=VECTOR ( 'NONE', #12933, 1000.000000000000114 ) ;
#1823=AXIS2_PLACEMENT_3D ( 'NONE', #9966, #8876, #203 ) ;
#1843=EDGE_CURVE ( 'NONE', #915, #2687, #631, .T. ) ;
#1880=EDGE_CURVE ( 'NONE', #1400, #5301, #9434, .T. ) ;
#1918=VERTEX_POINT ( 'NONE', #12111 ) ;
#1937=DIRECTION ( 'NONE',  ( 0.000000000000000000, -0.4999999999999993894, 0.8660254037844389297 ) ) ;
#1943=DIRECTION ( 'NONE',  ( -0.000000000000000000, 0.8660254037844390407, 0.4999999999999993339 ) ) ;
#1967=CIRCLE ( 'NONE', #2433, 2.041999999999999815 ) ;
#1968=ORIENTED_EDGE ( 'NONE', *, *, #13609, .F. ) ;
#2005=EDGE_CURVE ( 'NONE', #8555, #11820, #8573, .T. ) ;
#2034=CARTESIAN_POINT ( 'NONE',  ( 2.500000000000000000, -1.178949249685213863, 2.042000000000002924 ) ) ;
#2046=EDGE_LOOP ( 'NONE', ( #10992, #11416, #13574, #13696 ) ) ;
#2080=FACE_OUTER_BOUND ( 'NONE', #3791, .T. ) ;
#2085=CARTESIAN_POINT ( 'NONE',  ( 5.000000000000004441, 0.000000000000000000, 4.250000000000000000 ) ) ;
#2149=DIRECTION ( 'NONE',  ( -1.000000000000000000, -0.000000000000000000, -0.000000000000000000 ) ) ;
#2154=DIRECTION ( 'NONE',  ( 0.000000000000000000, 0.4999999999999993339, -0.8660254037844390407 ) ) ;
#2173=EDGE_LOOP ( 'NONE', ( #1242, #179 ) ) ;
#2178=DIRECTION ( 'NONE',  ( 1.000000000000000000, 0.000000000000000000, 0.000000000000000000 ) ) ;
#2192=ORIENTED_EDGE ( 'NONE', *, *, #5442, .F. ) ;
#2197=DIRECTION ( 'NONE',  ( 0.000000000000000000, -0.5000000000000011102, -0.8660254037844379305 ) ) ;
#2208=VERTEX_POINT ( 'NONE', #14179 ) ;
#2226=CYLINDRICAL_SURFACE ( 'NONE', #1529, 2.500000000000000888 ) ;
#2246=EDGE_CURVE ( 'NONE', #5301, #2366, #5556, .T. ) ;
#2274=LINE ( 'NONE', #8661, #6193 ) ;
#2278=ORIENTED_EDGE ( 'NONE', *, *, #10271, .T. ) ;
#2301=CARTESIAN_POINT ( 'NONE',  ( -31.74999999999995737, 0.000000000000000000, 0.000000000000000000 ) ) ;
#2315=CARTESIAN_POINT ( 'NONE',  ( 2.500000000000000000, -1.178949249685213863, 2.042000000000002924 ) ) ;
#2317=DIRECTION ( 'NONE',  ( 0.000000000000000000, 0.000000000000000000, -1.000000000000000000 ) ) ;
#2328=ADVANCED_FACE ( 'NONE', ( #9841 ), #14248, .F. ) ;
#2366=VERTEX_POINT ( 'NONE', #1398 ) ;
#2379=ORIENTED_EDGE ( 'NONE', *, *, #5447, .F. ) ;
#2386=EDGE_LOOP ( 'NONE', ( #13176, #9459 ) ) ;
#2410=EDGE_CURVE ( 'NONE', #3237, #12266, #1967, .T. ) ;
#2418=VERTEX_POINT ( 'NONE', #4540 ) ;
#2433=AXIS2_PLACEMENT_3D ( 'NONE', #9250, #3732, #10118 ) ;
#2492=CARTESIAN_POINT ( 'NONE',  ( 5.200000000000002842, 3.061616997868384127E-16, -2.500000000000000888 ) ) ;
#2500=VECTOR ( 'NONE', #9950, 1000.000000000000000 ) ;
#2502=ADVANCED_FACE ( 'NONE', ( #1014 ), #3376, .F. ) ;
#2510=ADVANCED_FACE ( 'NONE', ( #3508 ), #4297, .T. ) ;
#2522=EDGE_LOOP ( 'NONE', ( #5728, #3688, #4350, #7774 ) ) ;
#2542=VERTEX_POINT ( 'NONE', #939 ) ;
#2557=( NAMED_UNIT ( * ) PLANE_ANGLE_UNIT ( ) SI_UNIT ( $, .RADIAN. ) );
#2560=ORIENTED_EDGE ( 'NONE', *, *, #3697, .T. ) ;
#2562=ORIENTED_EDGE ( 'NONE', *, *, #14102, .T. ) ;
#2565=DIRECTION ( 'NONE',  ( 1.000000000000000000, 0.000000000000000000, 0.000000000000000000 ) ) ;
#2595=EDGE_CURVE ( 'NONE', #11820, #7879, #3234, .T. ) ;
#2606=EDGE_CURVE ( 'NONE', #4565, #7302, #10159, .T. ) ;
#2626=CARTESIAN_POINT ( 'NONE',  ( 5.200000000000002842, 0.000000000000000000, 0.000000000000000000 ) ) ;
#2631=SURFACE_STYLE_USAGE ( .BOTH. , #6030 ) ;
#2687=VERTEX_POINT ( 'NONE', #1378 ) ;
#2708=AXIS2_PLACEMENT_3D ( 'NONE', #12749, #5932, #9276 ) ;
#2735=FACE_OUTER_BOUND ( 'NONE', #1758, .T. ) ;
#2753=ORIENTED_EDGE ( 'NONE', *, *, #11673, .T. ) ;
#2762=AXIS2_PLACEMENT_3D ( 'NONE', #165, #236, #13458 ) ;
#2791=VECTOR ( 'NONE', #2154, 1000.000000000000000 ) ;
#2807=CARTESIAN_POINT ( 'NONE',  ( 2.500000000000000000, 2.357898499370433054, -1.951563910473907981E-15 ) ) ;
#2826=CARTESIAN_POINT ( 'NONE',  ( 5.200000000000002842, 3.306546357697854719E-16, 2.700000000000001066 ) ) ;
#2832=ORIENTED_EDGE ( 'NONE', *, *, #13056, .F. ) ;
#2865=CARTESIAN_POINT ( 'NONE',  ( 2.500000000000000000, 2.357898499370433054, -1.951563910473907981E-15 ) ) ;
#2900=ADVANCED_FACE ( 'NONE', ( #4000 ), #5585, .F. ) ;
#2911=DIRECTION ( 'NONE',  ( 0.000000000000000000, 0.000000000000000000, 1.000000000000000000 ) ) ;
#2922=ORIENTED_EDGE ( 'NONE', *, *, #980, .T. ) ;
#2936=FACE_OUTER_BOUND ( 'NONE', #6178, .T. ) ;
#2939=VECTOR ( 'NONE', #7088, 1000.000000000000000 ) ;
#2997=CARTESIAN_POINT ( 'NONE',  ( 5.200000000000002842, 0.000000000000000000, 0.000000000000000000 ) ) ;
#3011=DIRECTION ( 'NONE',  ( 0.000000000000000000, 0.000000000000000000, 1.000000000000000000 ) ) ;
#3017=VERTEX_POINT ( 'NONE', #7823 ) ;
#3036=CARTESIAN_POINT ( 'NONE',  ( -31.74999999999995737, 5.204748896376250699E-16, -4.250000000000000000 ) ) ;
#3050=ORIENTED_EDGE ( 'NONE', *, *, #5751, .T. ) ;
#3078=UNCERTAINTY_MEASURE_WITH_UNIT (LENGTH_MEASURE( 1.000000000000000082E-05 ), #5611, 'distance_accuracy_value', 'NONE');
#3086=DIRECTION ( 'NONE',  ( 0.000000000000000000, -0.4999999999999993894, 0.8660254037844389297 ) ) ;
#3112=LINE ( 'NONE', #12025, #2791 ) ;
#3117=EDGE_CURVE ( 'NONE', #5128, #1400, #4782, .T. ) ;
#3164=VERTEX_POINT ( 'NONE', #7089 ) ;
#3193=AXIS2_PLACEMENT_3D ( 'NONE', #3715, #133, #11264 ) ;
#3234=LINE ( 'NONE', #13224, #8069 ) ;
#3237=VERTEX_POINT ( 'NONE', #619 ) ;
#3258=MECHANICAL_DESIGN_GEOMETRIC_PRESENTATION_REPRESENTATION('',(#3737),#6722);
#3265=VECTOR ( 'NONE', #13513, 999.9999999999998863 ) ;
#3267=DIRECTION ( 'NONE',  ( 0.000000000000000000, -0.4999999999999992784, 0.8660254037844389297 ) ) ;
#3274=ORIENTED_EDGE ( 'NONE', *, *, #6302, .F. ) ;
#3299=CARTESIAN_POINT ( 'NONE',  ( 0.000000000000000000, -2.357898499370432610, 3.252606517456513302E-15 ) ) ;
#3333=EDGE_CURVE ( 'NONE', #3475, #4527, #1185, .T. ) ;
#3352=FACE_OUTER_BOUND ( 'NONE', #7813, .T. ) ;
#3368=ORIENTED_EDGE ( 'NONE', *, *, #13609, .T. ) ;
#3371=CARTESIAN_POINT ( 'NONE',  ( 0.2500000000000002220, 0.000000000000000000, 0.000000000000000000 ) ) ;
#3376=CONICAL_SURFACE ( 'NONE', #13535, 2.041999999999999815, 1.047197551196591858 ) ;
#3380=VERTEX_POINT ( 'NONE', #12367 ) ;
#3386=DIRECTION ( 'NONE',  ( 0.000000000000000000, 0.000000000000000000, 1.000000000000000000 ) ) ;
#3421=LINE ( 'NONE', #10078, #12546 ) ;
#3463=VECTOR ( 'NONE', #10584, 999.9999999999998863 ) ;
#3474=DIRECTION ( 'NONE',  ( 0.000000000000000000, -0.5000000000000011102, -0.8660254037844379305 ) ) ;
#3475=VERTEX_POINT ( 'NONE', #433 ) ;
#3508=FACE_OUTER_BOUND ( 'NONE', #2046, .T. ) ;
#3514=EDGE_LOOP ( 'NONE', ( #13682, #11484, #3274 ) ) ;
#3528=CONICAL_SURFACE ( 'NONE', #5353, 2.041999999999999815, 1.047197551196591858 ) ;
#3543=DIRECTION ( 'NONE',  ( 0.000000000000000000, 0.000000000000000000, 1.000000000000000000 ) ) ;
#3557=DIRECTION ( 'NONE',  ( 0.000000000000000000, -0.5000000000000012212, -0.8660254037844380415 ) ) ;
#3573=( NAMED_UNIT ( * ) SI_UNIT ( $, .STERADIAN. ) SOLID_ANGLE_UNIT ( ) );
#3588=DIRECTION ( 'NONE',  ( 0.000000000000000000, 0.000000000000000000, 1.000000000000000000 ) ) ;
#3590=CARTESIAN_POINT ( 'NONE',  ( 2.500000000000000000, 0.000000000000000000, 0.000000000000000000 ) ) ;
#3614=AXIS2_PLACEMENT_3D ( 'NONE', #4640, #9054, #12389 ) ;
#3619=CARTESIAN_POINT ( 'NONE',  ( 2.500000000000000000, 0.000000000000000000, 0.000000000000000000 ) ) ;
#3630=DIRECTION ( 'NONE',  ( -1.000000000000000000, -0.000000000000000000, -0.000000000000000000 ) ) ;
#3650=ORIENTED_EDGE ( 'NONE', *, *, #1694, .F. ) ;
#3676=PLANE ( 'NONE',  #8734 ) ;
#3677=EDGE_CURVE ( 'NONE', #7302, #8946, #6520, .T. ) ;
#3688=ORIENTED_EDGE ( 'NONE', *, *, #4327, .T. ) ;
#3697=EDGE_CURVE ( 'NONE', #4582, #4565, #10914, .T. ) ;
#3715=CARTESIAN_POINT ( 'NONE',  ( 2.500000000000000000, 2.357898499370433054, -1.951563910473907981E-15 ) ) ;
#3732=DIRECTION ( 'NONE',  ( -1.000000000000000000, -0.000000000000000000, -0.000000000000000000 ) ) ;
#3737=STYLED_ITEM('',(#14417),#3853);
#3771=PRODUCT_DEFINITION_FORMATION_WITH_SPECIFIED_SOURCE ( 'ANY', '', #11441, .NOT_KNOWN. ) ;
#3791=EDGE_LOOP ( 'NONE', ( #12631, #5458, #6276 ) ) ;
#3803=PLANE ( 'NONE',  #4842 ) ;
#3834=DIRECTION ( 'NONE',  ( -1.000000000000000000, -0.000000000000000000, -0.000000000000000000 ) ) ;
#3836=DIRECTION ( 'NONE',  ( 0.000000000000000000, 0.000000000000000000, -1.000000000000000000 ) ) ;
#3853=MANIFOLD_SOLID_BREP ( 'Hex', #12850 ) ;
#3905=ADVANCED_FACE ( 'NONE', ( #10611 ), #11586, .T. ) ;
#3933=DIRECTION ( 'NONE',  ( 1.000000000000000000, 0.000000000000000000, 0.000000000000000000 ) ) ;
#3940=CIRCLE ( 'NONE', #12049, 2.500000000000001332 ) ;
#3992=CARTESIAN_POINT ( 'NONE',  ( -31.74999999999995737, 0.000000000000000000, 2.500000000000000888 ) ) ;
#4000=FACE_OUTER_BOUND ( 'NONE', #3514, .T. ) ;
#4117=EDGE_CURVE ( 'NONE', #2687, #1127, #12482, .T. ) ;
#4149=EDGE_LOOP ( 'NONE', ( #13454, #6233, #12323, #6418, #11456 ) ) ;
#4194=PLANE ( 'NONE',  #5130 ) ;
#4200=EDGE_CURVE ( 'NONE', #8612, #12266, #13479, .T. ) ;
#4240=CARTESIAN_POINT ( 'NONE',  ( 2.500000000000000000, 1.178949249685218525, 2.041999999999999371 ) ) ;
#4263=ORIENTED_EDGE ( 'NONE', *, *, #7726, .T. ) ;
#4272=ORIENTED_EDGE ( 'NONE', *, *, #344, .F. ) ;
#4297=TOROIDAL_SURFACE ( 'NONE', #10786, 4.000000000000000000, 0.2500000000000000000 ) ;
#4317=PLANE ( 'NONE',  #10343 ) ;
#4322=DIRECTION ( 'NONE',  ( -1.000000000000000000, -0.000000000000000000, -0.000000000000000000 ) ) ;
#4327=EDGE_CURVE ( 'NONE', #2687, #2542, #404, .T. ) ;
#4347=VECTOR ( 'NONE', #14132, 1000.000000000000114 ) ;
#4350=ORIENTED_EDGE ( 'NONE', *, *, #8619, .F. ) ;
#4351=FACE_OUTER_BOUND ( 'NONE', #12084, .T. ) ;
#4395=EDGE_CURVE ( 'NONE', #12266, #722, #5362, .T. ) ;
#4408=ORIENTED_EDGE ( 'NONE', *, *, #825, .T. ) ;
#4464=MECHANICAL_DESIGN_GEOMETRIC_PRESENTATION_REPRESENTATION('',(#8860),#462);
#4501=PLANE ( 'NONE',  #9172 ) ;
#4527=VERTEX_POINT ( 'NONE', #9851 ) ;
#4540=CARTESIAN_POINT ( 'NONE',  ( 25.00000000000000000, 0.000000000000000000, 2.055000000000000160 ) ) ;
#4549=DIRECTION ( 'NONE',  ( -1.000000000000000000, -0.000000000000000000, -0.000000000000000000 ) ) ;
#4565=VERTEX_POINT ( 'NONE', #7595 ) ;
#4566=ORIENTED_EDGE ( 'NONE', *, *, #8079, .T. ) ;
#4582=VERTEX_POINT ( 'NONE', #2085 ) ;
#4583=DIRECTION ( 'NONE',  ( 0.000000000000000000, 0.000000000000000000, 1.000000000000000000 ) ) ;
#4630=EDGE_LOOP ( 'NONE', ( #4865, #2753, #7965, #4272 ) ) ;
#4640=CARTESIAN_POINT ( 'NONE',  ( 2.500000000000000000, 2.357898499370433054, -1.951563910473907981E-15 ) ) ;
#4654=LINE ( 'NONE', #11394, #8690 ) ;
#4678=CYLINDRICAL_SURFACE ( 'NONE', #838, 4.250000000000000000 ) ;
#4685=CARTESIAN_POINT ( 'NONE',  ( 3.678949249685231848, 0.000000000000000000, 0.000000000000000000 ) ) ;
#4698=ADVANCED_FACE ( 'NONE', ( #5703, #4845 ), #451, .T. ) ;
#4700=LINE ( 'NONE', #2034, #2500 ) ;
#4702=DIRECTION ( 'NONE',  ( -0.000000000000000000, 0.000000000000000000, 1.000000000000000000 ) ) ;
#4740=PLANE ( 'NONE',  #3193 ) ;
#4744=EDGE_LOOP ( 'NONE', ( #8129, #12177, #8340, #12813 ) ) ;
#4746=ORIENTED_EDGE ( 'NONE', *, *, #3117, .F. ) ;
#4769=VECTOR ( 'NONE', #3474, 1000.000000000000114 ) ;
#4777=ORIENTED_EDGE ( 'NONE', *, *, #4200, .T. ) ;
#4782=LINE ( 'NONE', #6951, #212 ) ;
#4786=CARTESIAN_POINT ( 'NONE',  ( 5.200000000000002842, 0.000000000000000000, 0.000000000000000000 ) ) ;
#4788=AXIS2_PLACEMENT_3D ( 'NONE', #10873, #9568, #13040 ) ;
#4793=DIRECTION ( 'NONE',  ( -1.000000000000000000, -0.000000000000000000, -0.000000000000000000 ) ) ;
#4822=DIRECTION ( 'NONE',  ( 0.000000000000000000, 0.000000000000000000, 1.000000000000000000 ) ) ;
#4823=ORIENTED_EDGE ( 'NONE', *, *, #1694, .T. ) ;
#4842=AXIS2_PLACEMENT_3D ( 'NONE', #11565, #6054, #6197 ) ;
#4845=FACE_OUTER_BOUND ( 'NONE', #2173, .T. ) ;
#4857=CARTESIAN_POINT ( 'NONE',  ( 2.500000000000000000, -1.178949249685213863, 2.042000000000002924 ) ) ;
#4865=ORIENTED_EDGE ( 'NONE', *, *, #12279, .F. ) ;
#4869=ORIENTED_EDGE ( 'NONE', *, *, #1007, .T. ) ;
#4870=DIRECTION ( 'NONE',  ( -1.000000000000000000, -0.000000000000000000, -0.000000000000000000 ) ) ;
#4885=DIRECTION ( 'NONE',  ( 0.000000000000000000, 0.000000000000000000, 1.000000000000000000 ) ) ;
#4887=CIRCLE ( 'NONE', #12986, 2.500000000000000888 ) ;
#4927=LINE ( 'NONE', #461, #7999 ) ;
#4960=ORIENTED_EDGE ( 'NONE', *, *, #11673, .F. ) ;
#5056=CIRCLE ( 'NONE', #1047, 2.041999999999999815 ) ;
#5077=DIRECTION ( 'NONE',  ( 1.000000000000000000, 0.000000000000000000, 0.000000000000000000 ) ) ;
#5098=CARTESIAN_POINT ( 'NONE',  ( 0.2500000000000002220, 0.000000000000000000, 0.000000000000000000 ) ) ;
#5104=CARTESIAN_POINT ( 'NONE',  ( 25.00000000000000000, 0.000000000000000000, 0.000000000000000000 ) ) ;
#5128=VERTEX_POINT ( 'NONE', #4685 ) ;
#5130=AXIS2_PLACEMENT_3D ( 'NONE', #8610, #8458, #681 ) ;
#5170=DIRECTION ( 'NONE',  ( -1.000000000000000000, -0.000000000000000000, -0.000000000000000000 ) ) ;
#5191=LINE ( 'NONE', #14089, #1775 ) ;
#5194=UNCERTAINTY_MEASURE_WITH_UNIT (LENGTH_MEASURE( 1.000000000000000082E-05 ), #5818, 'distance_accuracy_value', 'NONE');
#5221=DIRECTION ( 'NONE',  ( 0.000000000000000000, 1.000000000000000000, -1.224646799147353207E-16 ) ) ;
#5246=ORIENTED_EDGE ( 'NONE', *, *, #2606, .T. ) ;
#5282=TOROIDAL_SURFACE ( 'NONE', #10120, 2.700000000000001066, 0.2000000000000000111 ) ;
#5288=TOROIDAL_SURFACE ( 'NONE', #8026, 2.700000000000001066, 0.2000000000000000111 ) ;
#5301=VERTEX_POINT ( 'NONE', #9612 ) ;
#5307=LINE ( 'NONE', #9727, #4347 ) ;
#5312=VECTOR ( 'NONE', #3557, 999.9999999999998863 ) ;
#5326=ADVANCED_FACE ( 'NONE', ( #2936 ), #3803, .F. ) ;
#5353=AXIS2_PLACEMENT_3D ( 'NONE', #907, #11823, #13051 ) ;
#5359=CARTESIAN_POINT ( 'NONE',  ( 0.000000000000000000, 0.000000000000000000, 4.000000000000000000 ) ) ;
#5362=LINE ( 'NONE', #10736, #3463 ) ;
#5391=ORIENTED_EDGE ( 'NONE', *, *, #4327, .F. ) ;
#5405=CIRCLE ( 'NONE', #10966, 0.2000000000000000944 ) ;
#5442=EDGE_CURVE ( 'NONE', #7879, #8136, #2274, .T. ) ;
#5447=EDGE_CURVE ( 'NONE', #722, #4527, #5541, .T. ) ;
#5458=ORIENTED_EDGE ( 'NONE', *, *, #14291, .T. ) ;
#5461=CARTESIAN_POINT ( 'NONE',  ( 0.000000000000000000, 0.000000000000000000, 0.000000000000000000 ) ) ;
#5475=ORIENTED_EDGE ( 'NONE', *, *, #1609, .T. ) ;
#5488=DIRECTION ( 'NONE',  ( -1.000000000000000000, -0.000000000000000000, -0.000000000000000000 ) ) ;
#5526=ADVANCED_FACE ( 'NONE', ( #10244 ), #4740, .F. ) ;
#5541=LINE ( 'NONE', #1017, #6660 ) ;
#5546=ORIENTED_EDGE ( 'NONE', *, *, #263, .F. ) ;
#5552=CYLINDRICAL_SURFACE ( 'NONE', #710, 2.500000000000000888 ) ;
#5556=LINE ( 'NONE', #1032, #12051 ) ;
#5566=FACE_OUTER_BOUND ( 'NONE', #12830, .T. ) ;
#5585=PLANE ( 'NONE',  #12717 ) ;
#5598=VECTOR ( 'NONE', #11199, 1000.000000000000000 ) ;
#5611=( LENGTH_UNIT ( ) NAMED_UNIT ( * ) SI_UNIT ( .MILLI., .METRE. ) );
#5687=CARTESIAN_POINT ( 'NONE',  ( 0.000000000000000000, 2.357898499370433054, -1.951563910473907981E-15 ) ) ;
#5703=FACE_BOUND ( 'NONE', #2386, .T. ) ;
#5723=ADVANCED_FACE ( 'NONE', ( #415 ), #5288, .F. ) ;
#5728=ORIENTED_EDGE ( 'NONE', *, *, #4117, .F. ) ;
#5743=( NAMED_UNIT ( * ) PLANE_ANGLE_UNIT ( ) SI_UNIT ( $, .RADIAN. ) );
#5751=EDGE_CURVE ( 'NONE', #8946, #7668, #148, .T. ) ;
#5778=EDGE_CURVE ( 'NONE', #3164, #4582, #12909, .T. ) ;
#5815=CARTESIAN_POINT ( 'NONE',  ( 25.00000000000000000, 2.789133085058098087E-16, -2.055000000000000160 ) ) ;
#5818=( LENGTH_UNIT ( ) NAMED_UNIT ( * ) SI_UNIT ( .MILLI., .METRE. ) );
#5841=VECTOR ( 'NONE', #3630, 1000.000000000000000 ) ;
#5848=EDGE_CURVE ( 'NONE', #8299, #3017, #4700, .T. ) ;
#5865=EDGE_CURVE ( 'NONE', #8193, #3237, #5056, .T. ) ;
#5898=CARTESIAN_POINT ( 'NONE',  ( -31.74999999999995737, 0.000000000000000000, 0.000000000000000000 ) ) ;
#5907=DIRECTION ( 'NONE',  ( 0.000000000000000000, 0.000000000000000000, -1.000000000000000000 ) ) ;
#5932=DIRECTION ( 'NONE',  ( -1.000000000000000000, -0.000000000000000000, -0.000000000000000000 ) ) ;
#5959=VECTOR ( 'NONE', #3086, 1000.000000000000114 ) ;
#5975=CARTESIAN_POINT ( 'NONE',  ( 25.00000000000000000, 2.516649172247811061E-16, -2.055000000000000160 ) ) ;
#5999=CARTESIAN_POINT ( 'NONE',  ( 25.00000000000000000, 2.055000000000000160, 0.000000000000000000 ) ) ;
#6030=SURFACE_SIDE_STYLE ('',( #7046 ) ) ;
#6054=DIRECTION ( 'NONE',  ( 1.000000000000000000, 0.000000000000000000, 0.000000000000000000 ) ) ;
#6063=ORIENTED_EDGE ( 'NONE', *, *, #8900, .F. ) ;
#6118=LINE ( 'NONE', #7134, #6426 ) ;
#6178=EDGE_LOOP ( 'NONE', ( #755, #1968, #8335 ) ) ;
#6193=VECTOR ( 'NONE', #8806, 1000.000000000000000 ) ;
#6197=DIRECTION ( 'NONE',  ( 0.000000000000000000, 0.000000000000000000, -1.000000000000000000 ) ) ;
#6198=EDGE_LOOP ( 'NONE', ( #8683, #7258, #12979, #13330 ) ) ;
#6216=AXIS2_PLACEMENT_3D ( 'NONE', #6990, #11421, #3588 ) ;
#6233=ORIENTED_EDGE ( 'NONE', *, *, #10110, .F. ) ;
#6276=ORIENTED_EDGE ( 'NONE', *, *, #9528, .F. ) ;
#6302=EDGE_CURVE ( 'NONE', #1400, #8555, #8496, .T. ) ;
#6341=ORIENTED_EDGE ( 'NONE', *, *, #10658, .T. ) ;
#6395=CIRCLE ( 'NONE', #7075, 4.250000000000000000 ) ;
#6414=CARTESIAN_POINT ( 'NONE',  ( 0.2500000000000002220, 4.898587196589412829E-16, -4.000000000000000000 ) ) ;
#6418=ORIENTED_EDGE ( 'NONE', *, *, #14291, .F. ) ;
#6426=VECTOR ( 'NONE', #9460, 1000.000000000000000 ) ;
#6460=DIRECTION ( 'NONE',  ( 0.000000000000000000, 0.5000000000000011102, 0.8660254037844380415 ) ) ;
#6510=DIRECTION ( 'NONE',  ( -1.000000000000000000, -0.000000000000000000, -0.000000000000000000 ) ) ;
#6512=AXIS2_PLACEMENT_3D ( 'NONE', #6414, #803, #12863 ) ;
#6520=CIRCLE ( 'NONE', #6512, 0.2500000000000002220 ) ;
#6540=CARTESIAN_POINT ( 'NONE',  ( 2.500000000000000000, 0.000000000000000000, 0.000000000000000000 ) ) ;
#6576=PRODUCT_DEFINITION_SHAPE ( 'NONE', 'NONE',  #13043 ) ;
#6578=ORIENTED_EDGE ( 'NONE', *, *, #2005, .F. ) ;
#6590=EDGE_CURVE ( 'NONE', #2418, #915, #6118, .T. ) ;
#6593=PLANE ( 'NONE',  #13550 ) ;
#6600=CARTESIAN_POINT ( 'NONE',  ( 2.500000000000000000, 2.357898499370433054, -1.951563910473907981E-15 ) ) ;
#6602=DIRECTION ( 'NONE',  ( 0.000000000000000000, 0.000000000000000000, -1.000000000000000000 ) ) ;
#6656=DIRECTION ( 'NONE',  ( 0.000000000000000000, 0.000000000000000000, 1.000000000000000000 ) ) ;
#6660=VECTOR ( 'NONE', #10990, 1000.000000000000000 ) ;
#6722=( GEOMETRIC_REPRESENTATION_CONTEXT ( 3 ) GLOBAL_UNCERTAINTY_ASSIGNED_CONTEXT ( ( #5194 ) ) GLOBAL_UNIT_ASSIGNED_CONTEXT ( ( #5818, #2557, #11838 ) ) REPRESENTATION_CONTEXT ( 'NONE', 'WORKASPACE' ) );
#6757=DIRECTION ( 'NONE',  ( 0.000000000000000000, 0.000000000000000000, -1.000000000000000000 ) ) ;
#6893=ORIENTED_EDGE ( 'NONE', *, *, #12397, .T. ) ;
#6951=CARTESIAN_POINT ( 'NONE',  ( 2.500000000000000000, 2.500728763858895382E-16, -2.041999999999999815 ) ) ;
#6964=FACE_OUTER_BOUND ( 'NONE', #4630, .T. ) ;
#6972=DIRECTION ( 'NONE',  ( -1.000000000000000000, -0.000000000000000000, -0.000000000000000000 ) ) ;
#6975=CIRCLE ( 'NONE', #695, 2.055000000000000160 ) ;
#6990=CARTESIAN_POINT ( 'NONE',  ( 5.000000000000004441, 0.000000000000000000, 0.000000000000000000 ) ) ;
#7025=LINE ( 'NONE', #13533, #7781 ) ;
#7030=DIRECTION ( 'NONE',  ( 0.000000000000000000, 0.000000000000000000, 1.000000000000000000 ) ) ;
#7046=SURFACE_STYLE_FILL_AREA ( #8196 ) ;
#7075=AXIS2_PLACEMENT_3D ( 'NONE', #5098, #556, #10451 ) ;
#7080=PLANE ( 'NONE',  #10424 ) ;
#7088=DIRECTION ( 'NONE',  ( 0.000000000000000000, 1.000000000000000000, -1.471414886128461471E-15 ) ) ;
#7089=CARTESIAN_POINT ( 'NONE',  ( 5.000000000000004441, 5.204748896376250699E-16, -4.250000000000000000 ) ) ;
#7093=EDGE_CURVE ( 'NONE', #7302, #4565, #6395, .T. ) ;
#7116=VECTOR ( 'NONE', #423, 1000.000000000000000 ) ;
#7132=CARTESIAN_POINT ( 'NONE',  ( 2.500000000000000000, 1.768423874527822681, -1.021000000000002794 ) ) ;
#7134=CARTESIAN_POINT ( 'NONE',  ( 25.00000000000000000, 0.000000000000000000, 2.055000000000000160 ) ) ;
#7186=ORIENTED_EDGE ( 'NONE', *, *, #7468, .T. ) ;
#7258=ORIENTED_EDGE ( 'NONE', *, *, #3677, .T. ) ;
#7302=VERTEX_POINT ( 'NONE', #13399 ) ;
#7412=ORIENTED_EDGE ( 'NONE', *, *, #705, .T. ) ;
#7415=TOROIDAL_SURFACE ( 'NONE', #1136, 4.000000000000000000, 0.2500000000000000000 ) ;
#7425=LINE ( 'NONE', #2865, #5959 ) ;
#7446=DIRECTION ( 'NONE',  ( -1.000000000000000000, -0.000000000000000000, -0.000000000000000000 ) ) ;
#7451=DIRECTION ( 'NONE',  ( 0.000000000000000000, 1.000000000000000000, -1.287488025362403787E-15 ) ) ;
#7452=AXIS2_PLACEMENT_3D ( 'NONE', #3590, #7992, #12434 ) ;
#7468=EDGE_CURVE ( 'NONE', #7879, #8555, #4927, .T. ) ;
#7518=PLANE ( 'NONE',  #11842 ) ;
#7590=DIRECTION ( 'NONE',  ( -1.000000000000000000, -0.000000000000000000, -0.000000000000000000 ) ) ;
#7595=CARTESIAN_POINT ( 'NONE',  ( 0.2500000000000002220, 0.000000000000000000, 4.250000000000000000 ) ) ;
#7633=DIRECTION ( 'NONE',  ( 0.000000000000000000, 0.000000000000000000, 1.000000000000000000 ) ) ;
#7635=EDGE_CURVE ( 'NONE', #4565, #7668, #13127, .T. ) ;
#7668=VERTEX_POINT ( 'NONE', #5359 ) ;
#7707=CARTESIAN_POINT ( 'NONE',  ( -31.74999999999995737, 0.000000000000000000, 4.250000000000000000 ) ) ;
#7726=EDGE_CURVE ( 'NONE', #3475, #1918, #8460, .T. ) ;
#7736=DIRECTION ( 'NONE',  ( 0.000000000000000000, 0.000000000000000000, -1.000000000000000000 ) ) ;
#7749=LINE ( 'NONE', #12179, #8037 ) ;
#7752=DIRECTION ( 'NONE',  ( 0.000000000000000000, 1.000000000000000000, -1.471414886128461471E-15 ) ) ;
#7774=ORIENTED_EDGE ( 'NONE', *, *, #10658, .F. ) ;
#7781=VECTOR ( 'NONE', #10147, 1000.000000000000000 ) ;
#7810=ORIENTED_EDGE ( 'NONE', *, *, #4395, .T. ) ;
#7813=EDGE_LOOP ( 'NONE', ( #12804, #2379, #14201, #12130, #5475 ) ) ;
#7823=CARTESIAN_POINT ( 'NONE',  ( 0.000000000000000000, -1.178949249685213863, 2.042000000000002924 ) ) ;
#7834=LINE ( 'NONE', #11187, #13484 ) ;
#7835=ORIENTED_EDGE ( 'NONE', *, *, #6590, .F. ) ;
#7841=CARTESIAN_POINT ( 'NONE',  ( 2.500000000000000000, 3.004629197474318851E-15, 2.042000000000000259 ) ) ;
#7856=FACE_OUTER_BOUND ( 'NONE', #9650, .T. ) ;
#7874=ORIENTED_EDGE ( 'NONE', *, *, #7093, .T. ) ;
#7879=VERTEX_POINT ( 'NONE', #9848 ) ;
#7899=LINE ( 'NONE', #13551, #5841 ) ;
#7905=VECTOR ( 'NONE', #10016, 1000.000000000000000 ) ;
#7965=ORIENTED_EDGE ( 'NONE', *, *, #6590, .T. ) ;
#7992=DIRECTION ( 'NONE',  ( -1.000000000000000000, -0.000000000000000000, -0.000000000000000000 ) ) ;
#7999=VECTOR ( 'NONE', #12465, 1000.000000000000000 ) ;
#8026=AXIS2_PLACEMENT_3D ( 'NONE', #2997, #3933, #13787 ) ;
#8030=CIRCLE ( 'NONE', #13371, 2.700000000000001066 ) ;
#8037=VECTOR ( 'NONE', #10890, 1000.000000000000000 ) ;
#8054=( NAMED_UNIT ( * ) PLANE_ANGLE_UNIT ( ) SI_UNIT ( $, .RADIAN. ) );
#8069=VECTOR ( 'NONE', #2197, 1000.000000000000114 ) ;
#8079=EDGE_CURVE ( 'NONE', #7668, #8946, #12210, .T. ) ;
#8129=ORIENTED_EDGE ( 'NONE', *, *, #9818, .F. ) ;
#8136=VERTEX_POINT ( 'NONE', #3299 ) ;
#8137=DIRECTION ( 'NONE',  ( -0.000000000000000000, 1.471414886128461471E-15, 1.000000000000000000 ) ) ;
#8168=FACE_OUTER_BOUND ( 'NONE', #9897, .T. ) ;
#8193=VERTEX_POINT ( 'NONE', #7841 ) ;
#8196=FILL_AREA_STYLE ('',( #411 ) ) ;
#8223=ORIENTED_EDGE ( 'NONE', *, *, #1609, .F. ) ;
#8225=EDGE_CURVE ( 'NONE', #2418, #8279, #13142, .T. ) ;
#8277=DIRECTION ( 'NONE',  ( -1.000000000000000000, -0.000000000000000000, -0.000000000000000000 ) ) ;
#8278=AXIS2_PLACEMENT_3D ( 'NONE', #8491, #9449, #645 ) ;
#8279=VERTEX_POINT ( 'NONE', #5815 ) ;
#8286=FACE_OUTER_BOUND ( 'NONE', #13089, .T. ) ;
#8299=VERTEX_POINT ( 'NONE', #1304 ) ;
#8335=ORIENTED_EDGE ( 'NONE', *, *, #5865, .F. ) ;
#8340=ORIENTED_EDGE ( 'NONE', *, *, #1843, .T. ) ;
#8415=DIRECTION ( 'NONE',  ( -1.000000000000000000, -0.000000000000000000, -0.000000000000000000 ) ) ;
#8458=DIRECTION ( 'NONE',  ( 1.000000000000000000, 0.000000000000000000, 0.000000000000000000 ) ) ;
#8460=LINE ( 'NONE', #9783, #10116 ) ;
#8474=ORIENTED_EDGE ( 'NONE', *, *, #1880, .F. ) ;
#8491=CARTESIAN_POINT ( 'NONE',  ( 0.000000000000000000, 0.000000000000000000, 0.000000000000000000 ) ) ;
#8496=CIRCLE ( 'NONE', #13123, 2.041999999999999815 ) ;
#8537=EDGE_LOOP ( 'NONE', ( #7810, #11478, #11643 ) ) ;
#8541=PRODUCT_DEFINITION_CONTEXT ( 'detailed design', #12764, 'design' ) ;
#8555=VERTEX_POINT ( 'NONE', #182 ) ;
#8573=CIRCLE ( 'NONE', #13431, 2.041999999999999815 ) ;
#8610=CARTESIAN_POINT ( 'NONE',  ( 2.500000000000000000, 2.357898499370433054, -1.951563910473907981E-15 ) ) ;
#8612=VERTEX_POINT ( 'NONE', #8850 ) ;
#8619=EDGE_CURVE ( 'NONE', #2208, #2542, #8030, .T. ) ;
#8661=CARTESIAN_POINT ( 'NONE',  ( 2.500000000000000000, -2.357898499370432610, 3.252606517456513302E-15 ) ) ;
#8683=ORIENTED_EDGE ( 'NONE', *, *, #7093, .F. ) ;
#8686=EDGE_CURVE ( 'NONE', #8193, #13622, #13615, .T. ) ;
#8690=VECTOR ( 'NONE', #9212, 1000.000000000000114 ) ;
#8703=PLANE ( 'NONE',  #9209 ) ;
#8714=ADVANCED_FACE ( 'NONE', ( #9200 ), #1492, .T. ) ;
#8734=AXIS2_PLACEMENT_3D ( 'NONE', #2807, #9259, #1409 ) ;
#8738=DIRECTION ( 'NONE',  ( 0.000000000000000000, -1.000000000000000000, 0.000000000000000000 ) ) ;
#8764=CIRCLE ( 'NONE', #6216, 4.250000000000000000 ) ;
#8767=CARTESIAN_POINT ( 'NONE',  ( 2.500000000000000000, -2.357898499370432610, 3.252606517456513302E-15 ) ) ;
#8806=DIRECTION ( 'NONE',  ( -1.000000000000000000, -0.000000000000000000, -0.000000000000000000 ) ) ;
#8849=DIRECTION ( 'NONE',  ( 0.000000000000000000, 0.8660254037844380415, -0.5000000000000011102 ) ) ;
#8850=CARTESIAN_POINT ( 'NONE',  ( 2.500000000000000000, 2.357898499370433054, -1.951563910473907981E-15 ) ) ;
#8860=STYLED_ITEM ( 'NONE', ( #337 ), #1425 ) ;
#8876=DIRECTION ( 'NONE',  ( 1.000000000000000000, 0.000000000000000000, 0.000000000000000000 ) ) ;
#8899=ADVANCED_FACE ( 'NONE', ( #13386 ), #2226, .T. ) ;
#8900=EDGE_CURVE ( 'NONE', #2542, #2208, #827, .T. ) ;
#8924=CARTESIAN_POINT ( 'NONE',  ( -31.74999999999995737, 3.061616997868384127E-16, -2.500000000000000888 ) ) ;
#8946=VERTEX_POINT ( 'NONE', #1119 ) ;
#8971=ADVANCED_FACE ( 'NONE', ( #1265, #5566 ), #1197, .T. ) ;
#9049=ADVANCED_FACE ( 'NONE', ( #2735 ), #3676, .F. ) ;
#9054=DIRECTION ( 'NONE',  ( 0.000000000000000000, -0.8660254037844390407, -0.4999999999999994449 ) ) ;
#9094=ORIENTED_EDGE ( 'NONE', *, *, #980, .F. ) ;
#9125=EDGE_LOOP ( 'NONE', ( #9094, #9723, #2560, #5246 ) ) ;
#9147=DIRECTION ( 'NONE',  ( 0.000000000000000000, 0.000000000000000000, 1.000000000000000000 ) ) ;
#9169=CARTESIAN_POINT ( 'NONE',  ( 2.500000000000000000, 2.357898499370433054, -1.951563910473907981E-15 ) ) ;
#9172=AXIS2_PLACEMENT_3D ( 'NONE', #2315, #8849, #6460 ) ;
#9200=FACE_OUTER_BOUND ( 'NONE', #9125, .T. ) ;
#9209=AXIS2_PLACEMENT_3D ( 'NONE', #6600, #11031, #1061 ) ;
#9212=DIRECTION ( 'NONE',  ( -0.5000000000000051070, 0.000000000000000000, 0.8660254037844355990 ) ) ;
#9250=CARTESIAN_POINT ( 'NONE',  ( 2.500000000000000000, 0.000000000000000000, 0.000000000000000000 ) ) ;
#9257=ORIENTED_EDGE ( 'NONE', *, *, #9935, .F. ) ;
#9259=DIRECTION ( 'NONE',  ( 1.000000000000000000, 0.000000000000000000, 0.000000000000000000 ) ) ;
#9265=ADVANCED_FACE ( 'NONE', ( #7856 ), #5552, .T. ) ;
#9276=DIRECTION ( 'NONE',  ( 0.000000000000000000, 0.000000000000000000, 1.000000000000000000 ) ) ;
#9289=ORIENTED_EDGE ( 'NONE', *, *, #2595, .T. ) ;
#9292=ORIENTED_EDGE ( 'NONE', *, *, #2246, .T. ) ;
#9313=ORIENTED_EDGE ( 'NONE', *, *, #12397, .F. ) ;
#9372=( NAMED_UNIT ( * ) SI_UNIT ( $, .STERADIAN. ) SOLID_ANGLE_UNIT ( ) );
#9418=DIRECTION ( 'NONE',  ( 0.000000000000000000, 0.000000000000000000, 1.000000000000000000 ) ) ;
#9434=LINE ( 'NONE', #13845, #10902 ) ;
#9442=ORIENTED_EDGE ( 'NONE', *, *, #5442, .T. ) ;
#9449=DIRECTION ( 'NONE',  ( -1.000000000000000000, -0.000000000000000000, -0.000000000000000000 ) ) ;
#9458=FACE_OUTER_BOUND ( 'NONE', #9974, .T. ) ;
#9459=ORIENTED_EDGE ( 'NONE', *, *, #8900, .T. ) ;
#9460=DIRECTION ( 'NONE',  ( -0.7071067811865306973, 0.000000000000000000, 0.7071067811865643371 ) ) ;
#9519=SHAPE_DEFINITION_REPRESENTATION ( #6576, #13104 ) ;
#9528=EDGE_CURVE ( 'NONE', #11820, #8193, #13695, .T. ) ;
#9568=DIRECTION ( 'NONE',  ( 0.000000000000000000, -1.000000000000000000, 0.000000000000000000 ) ) ;
#9588=ORIENTED_EDGE ( 'NONE', *, *, #8225, .F. ) ;
#9612=CARTESIAN_POINT ( 'NONE',  ( 2.500000000000000000, -1.178949249685218303, -2.041999999999998039 ) ) ;
#9650=EDGE_LOOP ( 'NONE', ( #4408, #632, #11252, #14155 ) ) ;
#9659=AXIS2_PLACEMENT_3D ( 'NONE', #12236, #10062, #7736 ) ;
#9723=ORIENTED_EDGE ( 'NONE', *, *, #5778, .T. ) ;
#9727=CARTESIAN_POINT ( 'NONE',  ( 2.500000000000000000, 2.357898499370433054, -1.951563910473907981E-15 ) ) ;
#9783=CARTESIAN_POINT ( 'NONE',  ( 0.000000000000000000, 2.357898499370433054, -1.951563910473907981E-15 ) ) ;
#9792=ORIENTED_EDGE ( 'NONE', *, *, #8225, .T. ) ;
#9818=EDGE_CURVE ( 'NONE', #3380, #1127, #11384, .T. ) ;
#9832=CARTESIAN_POINT ( 'NONE',  ( 2.500000000000000000, -1.178949249685213863, 2.042000000000002924 ) ) ;
#9841=FACE_OUTER_BOUND ( 'NONE', #8537, .T. ) ;
#9848=CARTESIAN_POINT ( 'NONE',  ( 2.500000000000000000, -2.357898499370432610, 3.252606517456513302E-15 ) ) ;
#9851=CARTESIAN_POINT ( 'NONE',  ( 0.000000000000000000, 1.178949249685213863, -2.042000000000001148 ) ) ;
#9890=DIRECTION ( 'NONE',  ( -1.000000000000000000, -0.000000000000000000, -0.000000000000000000 ) ) ;
#9893=DIRECTION ( 'NONE',  ( -1.000000000000000000, -0.000000000000000000, -0.000000000000000000 ) ) ;
#9897=EDGE_LOOP ( 'NONE', ( #9588, #4960 ) ) ;
#9920=DIRECTION ( 'NONE',  ( 0.000000000000000000, 0.000000000000000000, 1.000000000000000000 ) ) ;
#9935=EDGE_CURVE ( 'NONE', #3017, #1918, #3421, .T. ) ;
#9950=DIRECTION ( 'NONE',  ( -1.000000000000000000, -0.000000000000000000, -0.000000000000000000 ) ) ;
#9966=CARTESIAN_POINT ( 'NONE',  ( 0.2500000000000002220, 0.000000000000000000, 0.000000000000000000 ) ) ;
#9974=EDGE_LOOP ( 'NONE', ( #5391, #13918, #6341, #6063 ) ) ;
#9996=CARTESIAN_POINT ( 'NONE',  ( 0.000000000000000000, 0.000000000000000000, 0.000000000000000000 ) ) ;
#10016=DIRECTION ( 'NONE',  ( -1.000000000000000000, -0.000000000000000000, -0.000000000000000000 ) ) ;
#10057=ORIENTED_EDGE ( 'NONE', *, *, #5447, .T. ) ;
#10061=EDGE_LOOP ( 'NONE', ( #9792, #13645, #13082, #7835 ) ) ;
#10062=DIRECTION ( 'NONE',  ( -1.000000000000000000, -0.000000000000000000, -0.000000000000000000 ) ) ;
#10075=AXIS2_PLACEMENT_3D ( 'NONE', #9169, #13589, #5907 ) ;
#10078=CARTESIAN_POINT ( 'NONE',  ( 0.000000000000000000, -1.178949249685213863, 2.042000000000002924 ) ) ;
#10088=CARTESIAN_POINT ( 'NONE',  ( 25.00000000000000000, 0.000000000000000000, 0.000000000000000000 ) ) ;
#10110=EDGE_CURVE ( 'NONE', #13622, #1918, #230, .T. ) ;
#10116=VECTOR ( 'NONE', #1937, 1000.000000000000114 ) ;
#10118=DIRECTION ( 'NONE',  ( 0.000000000000000000, 0.000000000000000000, 1.000000000000000000 ) ) ;
#10120=AXIS2_PLACEMENT_3D ( 'NONE', #2626, #1082, #6757 ) ;
#10147=DIRECTION ( 'NONE',  ( 0.000000000000000000, 1.000000000000000000, -1.471414886128461471E-15 ) ) ;
#10159=CIRCLE ( 'NONE', #1823, 4.250000000000000000 ) ;
#10200=DIRECTION ( 'NONE',  ( -1.000000000000000000, 0.000000000000000000, -0.000000000000000000 ) ) ;
#10214=ORIENTED_EDGE ( 'NONE', *, *, #2246, .F. ) ;
#10244=FACE_OUTER_BOUND ( 'NONE', #80, .T. ) ;
#10271=EDGE_CURVE ( 'NONE', #8555, #5301, #12651, .T. ) ;
#10286=DIRECTION ( 'NONE',  ( -0.5000000000000051070, 1.060575238724903217E-16, -0.8660254037844355990 ) ) ;
#10295=CARTESIAN_POINT ( 'NONE',  ( 24.55500000000002103, 0.000000000000000000, 0.000000000000000000 ) ) ;
#10343=AXIS2_PLACEMENT_3D ( 'NONE', #9832, #8137, #11556 ) ;
#10376=ORIENTED_EDGE ( 'NONE', *, *, #5865, .T. ) ;
#10424=AXIS2_PLACEMENT_3D ( 'NONE', #5999, #10427, #457 ) ;
#10427=DIRECTION ( 'NONE',  ( 1.000000000000000000, 0.000000000000000000, 0.000000000000000000 ) ) ;
#10439=DIRECTION ( 'NONE',  ( 1.000000000000000000, 0.000000000000000000, 0.000000000000000000 ) ) ;
#10451=DIRECTION ( 'NONE',  ( 0.000000000000000000, 0.000000000000000000, 1.000000000000000000 ) ) ;
#10461=CARTESIAN_POINT ( 'NONE',  ( 5.000000000000004441, 0.000000000000000000, 0.000000000000000000 ) ) ;
#10508=CARTESIAN_POINT ( 'NONE',  ( 0.000000000000000000, 0.000000000000000000, 0.000000000000000000 ) ) ;
#10569=CARTESIAN_POINT ( 'NONE',  ( 2.500000000000000000, 0.000000000000000000, 0.000000000000000000 ) ) ;
#10584=DIRECTION ( 'NONE',  ( 0.000000000000000000, -0.5000000000000012212, -0.8660254037844380415 ) ) ;
#10611=FACE_OUTER_BOUND ( 'NONE', #10061, .T. ) ;
#10638=CARTESIAN_POINT ( 'NONE',  ( 2.500000000000000000, -2.357898499370432610, 3.252606517456513302E-15 ) ) ;
#10650=CARTESIAN_POINT ( 'NONE',  ( 24.55500000000002103, 0.000000000000000000, 2.500000000000001332 ) ) ;
#10652=FACE_OUTER_BOUND ( 'NONE', #7, .T. ) ;
#10658=EDGE_CURVE ( 'NONE', #1127, #2208, #5405, .T. ) ;
#10723=CONICAL_SURFACE ( 'NONE', #1198, 2.055000000000000160, 0.7853981633974721488 ) ;
#10730=ADVANCED_FACE ( 'NONE', ( #1278 ), #13688, .T. ) ;
#10736=CARTESIAN_POINT ( 'NONE',  ( 2.500000000000000000, 2.357898499370433054, -1.951563910473907981E-15 ) ) ;
#10764=EDGE_LOOP ( 'NONE', ( #4746, #1526, #10376, #13065, #2562 ) ) ;
#10786=AXIS2_PLACEMENT_3D ( 'NONE', #3371, #12204, #7633 ) ;
#10794=ORIENTED_EDGE ( 'NONE', *, *, #10110, .T. ) ;
#10826=DIRECTION ( 'NONE',  ( 0.000000000000000000, 0.000000000000000000, 1.000000000000000000 ) ) ;
#10829=ORIENTED_EDGE ( 'NONE', *, *, #2595, .F. ) ;
#10850=ORIENTED_EDGE ( 'NONE', *, *, #3117, .T. ) ;
#10873=CARTESIAN_POINT ( 'NONE',  ( 0.2500000000000002220, 0.000000000000000000, 4.000000000000000000 ) ) ;
#10890=DIRECTION ( 'NONE',  ( 0.000000000000000000, -1.000000000000000000, 1.287488025362403787E-15 ) ) ;
#10902=VECTOR ( 'NONE', #14128, 1000.000000000000000 ) ;
#10914=LINE ( 'NONE', #7707, #5598 ) ;
#10966=AXIS2_PLACEMENT_3D ( 'NONE', #11067, #8738, #12142 ) ;
#10990=DIRECTION ( 'NONE',  ( -1.000000000000000000, -0.000000000000000000, -0.000000000000000000 ) ) ;
#10992=ORIENTED_EDGE ( 'NONE', *, *, #3677, .F. ) ;
#11005=CARTESIAN_POINT ( 'NONE',  ( 5.200000000000002842, 0.000000000000000000, 0.000000000000000000 ) ) ;
#11017=ADVANCED_FACE ( 'NONE', ( #4351 ), #3528, .F. ) ;
#11021=EDGE_LOOP ( 'NONE', ( #9313, #11203, #7412, #9289, #9442 ) ) ;
#11031=DIRECTION ( 'NONE',  ( 0.000000000000000000, 0.8660254037844380415, -0.5000000000000012212 ) ) ;
#11067=CARTESIAN_POINT ( 'NONE',  ( 5.200000000000002842, 0.000000000000000000, -2.700000000000001066 ) ) ;
#11080=CIRCLE ( 'NONE', #11730, 2.041999999999999815 ) ;
#11109=CARTESIAN_POINT ( 'NONE',  ( 2.500000000000000000, 2.357898499370433054, -1.951563910473907981E-15 ) ) ;
#11133=VECTOR ( 'NONE', #698, 1000.000000000000000 ) ;
#11137=ORIENTED_EDGE ( 'NONE', *, *, #13056, .T. ) ;
#11162=CARTESIAN_POINT ( 'NONE',  ( 24.55500000000002103, 0.000000000000000000, 0.000000000000000000 ) ) ;
#11187=CARTESIAN_POINT ( 'NONE',  ( 0.000000000000000000, 1.178949249685213863, -2.042000000000001148 ) ) ;
#11199=DIRECTION ( 'NONE',  ( -1.000000000000000000, -0.000000000000000000, -0.000000000000000000 ) ) ;
#11203=ORIENTED_EDGE ( 'NONE', *, *, #5848, .F. ) ;
#11252=ORIENTED_EDGE ( 'NONE', *, *, #1162, .T. ) ;
#11264=DIRECTION ( 'NONE',  ( 0.000000000000000000, 0.000000000000000000, -1.000000000000000000 ) ) ;
#11384=LINE ( 'NONE', #8924, #7905 ) ;
#11393=ADVANCED_FACE ( 'NONE', ( #2080 ), #4194, .F. ) ;
#11394=CARTESIAN_POINT ( 'NONE',  ( 2.500000000000000000, 0.000000000000000000, 2.041999999999999815 ) ) ;
#11416=ORIENTED_EDGE ( 'NONE', *, *, #2606, .F. ) ;
#11421=DIRECTION ( 'NONE',  ( -1.000000000000000000, -0.000000000000000000, -0.000000000000000000 ) ) ;
#11441=PRODUCT ( 'socket head cap screw_iso_ISO 4762 M5 x 20 - 20N', 'socket head cap screw_iso_ISO 4762 M5 x 20 - 20N', '', ( #414 ) ) ;
#11456=ORIENTED_EDGE ( 'NONE', *, *, #5848, .T. ) ;
#11471=ORIENTED_EDGE ( 'NONE', *, *, #6302, .T. ) ;
#11478=ORIENTED_EDGE ( 'NONE', *, *, #14251, .T. ) ;
#11484=ORIENTED_EDGE ( 'NONE', *, *, #10271, .F. ) ;
#11494=ADVANCED_FACE ( 'NONE', ( #10652 ), #7518, .F. ) ;
#11556=DIRECTION ( 'NONE',  ( 0.000000000000000000, -1.000000000000000000, 1.471414886128461471E-15 ) ) ;
#11565=CARTESIAN_POINT ( 'NONE',  ( 2.500000000000000000, 2.357898499370433054, -1.951563910473907981E-15 ) ) ;
#11586=CONICAL_SURFACE ( 'NONE', #13433, 2.055000000000000160, 0.7853981633974721488 ) ;
#11643=ORIENTED_EDGE ( 'NONE', *, *, #14102, .F. ) ;
#11673=EDGE_CURVE ( 'NONE', #8279, #2418, #6975, .T. ) ;
#11730=AXIS2_PLACEMENT_3D ( 'NONE', #12839, #5170, #2911 ) ;
#11763=UNCERTAINTY_MEASURE_WITH_UNIT (LENGTH_MEASURE( 1.000000000000000082E-05 ), #13639, 'distance_accuracy_value', 'NONE');
#11796=AXIS2_PLACEMENT_3D ( 'NONE', #2826, #5221, #11815 ) ;
#11815=DIRECTION ( 'NONE',  ( 0.000000000000000000, 1.224646799147353207E-16, 1.000000000000000000 ) ) ;
#11820=VERTEX_POINT ( 'NONE', #12650 ) ;
#11823=DIRECTION ( 'NONE',  ( -1.000000000000000000, -0.000000000000000000, -0.000000000000000000 ) ) ;
#11838=( NAMED_UNIT ( * ) SI_UNIT ( $, .STERADIAN. ) SOLID_ANGLE_UNIT ( ) );
#11842=AXIS2_PLACEMENT_3D ( 'NONE', #12888, #13974, #7451 ) ;
#11955=ORIENTED_EDGE ( 'NONE', *, *, #3697, .F. ) ;
#12025=CARTESIAN_POINT ( 'NONE',  ( 0.000000000000000000, -2.357898499370432610, 3.252606517456513302E-15 ) ) ;
#12033=APPLICATION_CONTEXT ( 'automotive_design' ) ;
#12049=AXIS2_PLACEMENT_3D ( 'NONE', #11162, #33, #3543 ) ;
#12051=VECTOR ( 'NONE', #2149, 1000.000000000000000 ) ;
#12084=EDGE_LOOP ( 'NONE', ( #5546, #10850, #11471, #13973, #12479 ) ) ;
#12103=VECTOR ( 'NONE', #1700, 1000.000000000000000 ) ;
#12111=CARTESIAN_POINT ( 'NONE',  ( 0.000000000000000000, 1.178949249685218525, 2.041999999999999371 ) ) ;
#12130=ORIENTED_EDGE ( 'NONE', *, *, #4200, .F. ) ;
#12142=DIRECTION ( 'NONE',  ( 0.000000000000000000, 0.000000000000000000, -1.000000000000000000 ) ) ;
#12147=CARTESIAN_POINT ( 'NONE',  ( -31.74999999999995737, 0.000000000000000000, 0.000000000000000000 ) ) ;
#12156=ADVANCED_FACE ( 'NONE', ( #13298 ), #4317, .F. ) ;
#12172=EDGE_LOOP ( 'NONE', ( #4263, #9257, #6893, #4869, #3650, #13216 ) ) ;
#12177=ORIENTED_EDGE ( 'NONE', *, *, #344, .T. ) ;
#12179=CARTESIAN_POINT ( 'NONE',  ( 2.500000000000000000, 1.178949249685213863, -2.042000000000001148 ) ) ;
#12204=DIRECTION ( 'NONE',  ( -1.000000000000000000, -0.000000000000000000, -0.000000000000000000 ) ) ;
#12210=CIRCLE ( 'NONE', #12901, 4.000000000000000000 ) ;
#12236=CARTESIAN_POINT ( 'NONE',  ( 5.000000000000000888, 0.000000000000000000, 0.000000000000000000 ) ) ;
#12255=DIRECTION ( 'NONE',  ( -1.000000000000000000, -0.000000000000000000, -0.000000000000000000 ) ) ;
#12257=ADVANCED_FACE ( 'NONE', ( #8286 ), #4678, .T. ) ;
#12266=VERTEX_POINT ( 'NONE', #7132 ) ;
#12267=DIRECTION ( 'NONE',  ( 0.000000000000000000, 0.000000000000000000, 1.000000000000000000 ) ) ;
#12278=CARTESIAN_POINT ( 'NONE',  ( 25.00000000000000000, 0.000000000000000000, 0.000000000000000000 ) ) ;
#12279=EDGE_CURVE ( 'NONE', #8279, #3380, #1604, .T. ) ;
#12315=CARTESIAN_POINT ( 'NONE',  ( 2.500000000000000000, 1.178949249685213863, -2.042000000000001148 ) ) ;
#12323=ORIENTED_EDGE ( 'NONE', *, *, #8686, .F. ) ;
#12367=CARTESIAN_POINT ( 'NONE',  ( 24.55500000000002103, 3.061616997868384620E-16, -2.500000000000001332 ) ) ;
#12389=DIRECTION ( 'NONE',  ( 0.000000000000000000, 0.4999999999999993894, -0.8660254037844389297 ) ) ;
#12397=EDGE_CURVE ( 'NONE', #3017, #8136, #5191, .T. ) ;
#12434=DIRECTION ( 'NONE',  ( 0.000000000000000000, 0.000000000000000000, 1.000000000000000000 ) ) ;
#12456=AXIS2_PLACEMENT_3D ( 'NONE', #10461, #8277, #4885 ) ;
#12460=CARTESIAN_POINT ( 'NONE',  ( 2.500000000000000000, -1.178949249685213863, 2.042000000000002924 ) ) ;
#12465=DIRECTION ( 'NONE',  ( 0.000000000000000000, 0.4999999999999993339, -0.8660254037844390407 ) ) ;
#12479=ORIENTED_EDGE ( 'NONE', *, *, #9528, .T. ) ;
#12482=CIRCLE ( 'NONE', #651, 2.500000000000000888 ) ;
#12500=ADVANCED_FACE ( 'NONE', ( #9458 ), #5282, .F. ) ;
#12546=VECTOR ( 'NONE', #7752, 1000.000000000000000 ) ;
#12552=DIRECTION ( 'NONE',  ( 0.000000000000000000, -1.000000000000000000, 1.287488025362403787E-15 ) ) ;
#12631=ORIENTED_EDGE ( 'NONE', *, *, #705, .F. ) ;
#12650=CARTESIAN_POINT ( 'NONE',  ( 2.500000000000000000, -1.768423874527823569, 1.021000000000002794 ) ) ;
#12651=LINE ( 'NONE', #10638, #12103 ) ;
#12717=AXIS2_PLACEMENT_3D ( 'NONE', #11109, #2178, #6602 ) ;
#12749=CARTESIAN_POINT ( 'NONE',  ( -31.74999999999995737, 0.000000000000000000, 0.000000000000000000 ) ) ;
#12764=APPLICATION_CONTEXT ( 'automotive_design' ) ;
#12804=ORIENTED_EDGE ( 'NONE', *, *, #3333, .T. ) ;
#12813=ORIENTED_EDGE ( 'NONE', *, *, #4117, .T. ) ;
#12818=DIRECTION ( 'NONE',  ( 0.000000000000000000, 0.000000000000000000, 1.000000000000000000 ) ) ;
#12830=EDGE_LOOP ( 'NONE', ( #4566, #3050 ) ) ;
#12839=CARTESIAN_POINT ( 'NONE',  ( 2.500000000000000000, 0.000000000000000000, 0.000000000000000000 ) ) ;
#12850=CLOSED_SHELL ( 'NONE', ( #11017, #1030, #5723, #12257, #9265, #3905, #8971, #966, #1535, #8899, #4698, #8714, #12500, #2510, #10730, #12156, #14260, #618, #11494, #14258, #2900, #5526, #11393, #5326, #9049, #2328, #2502 ) ) ;
#12860=AXIS2_PLACEMENT_3D ( 'NONE', #10295, #4793, #12267 ) ;
#12863=DIRECTION ( 'NONE',  ( 0.000000000000000000, -1.224646799147353454E-16, 1.000000000000000000 ) ) ;
#12888=CARTESIAN_POINT ( 'NONE',  ( 2.500000000000000000, 1.178949249685213863, -2.042000000000001148 ) ) ;
#12901=AXIS2_PLACEMENT_3D ( 'NONE', #5461, #9890, #3011 ) ;
#12909=CIRCLE ( 'NONE', #12456, 4.250000000000000000 ) ;
#12933=DIRECTION ( 'NONE',  ( 0.000000000000000000, -0.5000000000000011102, -0.8660254037844379305 ) ) ;
#12979=ORIENTED_EDGE ( 'NONE', *, *, #8079, .F. ) ;
#12986=AXIS2_PLACEMENT_3D ( 'NONE', #11005, #2565, #1528 ) ;
#13002=ORIENTED_EDGE ( 'NONE', *, *, #13470, .T. ) ;
#13034=LINE ( 'NONE', #3036, #13659 ) ;
#13040=DIRECTION ( 'NONE',  ( 0.000000000000000000, 0.000000000000000000, -1.000000000000000000 ) ) ;
#13043=PRODUCT_DEFINITION ( 'UNKNOWN', '', #3771, #8541 ) ;
#13049=FACE_OUTER_BOUND ( 'NONE', #13349, .T. ) ;
#13051=DIRECTION ( 'NONE',  ( 0.000000000000000000, 0.000000000000000000, 1.000000000000000000 ) ) ;
#13056=EDGE_CURVE ( 'NONE', #8612, #3237, #5307, .T. ) ;
#13065=ORIENTED_EDGE ( 'NONE', *, *, #2410, .T. ) ;
#13069=CARTESIAN_POINT ( 'NONE',  ( 2.500000000000000000, -2.629050547790028551E-15, -2.041999999999999815 ) ) ;
#13082=ORIENTED_EDGE ( 'NONE', *, *, #825, .F. ) ;
#13089=EDGE_LOOP ( 'NONE', ( #13002, #2922, #7874, #11955 ) ) ;
#13097=CARTESIAN_POINT ( 'NONE',  ( 0.2500000000000002220, 0.000000000000000000, 0.000000000000000000 ) ) ;
#13104=SHAPE_REPRESENTATION ( 'socket head cap screw_iso_ISO 4762 M5 x 20 - 20N', ( #14039 ), #731 ) ;
#13123=AXIS2_PLACEMENT_3D ( 'NONE', #3619, #3834, #7030 ) ;
#13127=CIRCLE ( 'NONE', #4788, 0.2500000000000002220 ) ;
#13142=CIRCLE ( 'NONE', #13823, 2.055000000000000160 ) ;
#13176=ORIENTED_EDGE ( 'NONE', *, *, #8619, .T. ) ;
#13193=ORIENTED_EDGE ( 'NONE', *, *, #14251, .F. ) ;
#13216=ORIENTED_EDGE ( 'NONE', *, *, #3333, .F. ) ;
#13224=CARTESIAN_POINT ( 'NONE',  ( 2.500000000000000000, -1.178949249685213863, 2.042000000000002924 ) ) ;
#13298=FACE_OUTER_BOUND ( 'NONE', #4149, .T. ) ;
#13330=ORIENTED_EDGE ( 'NONE', *, *, #7635, .F. ) ;
#13349=EDGE_LOOP ( 'NONE', ( #14239, #2192, #7186, #2278, #9292 ) ) ;
#13371=AXIS2_PLACEMENT_3D ( 'NONE', #105, #12255, #2317 ) ;
#13386=FACE_OUTER_BOUND ( 'NONE', #4744, .T. ) ;
#13399=CARTESIAN_POINT ( 'NONE',  ( 0.2500000000000002220, 5.204748896376250699E-16, -4.250000000000000000 ) ) ;
#13431=AXIS2_PLACEMENT_3D ( 'NONE', #10569, #7446, #12818 ) ;
#13433=AXIS2_PLACEMENT_3D ( 'NONE', #5104, #8415, #562 ) ;
#13437=EDGE_LOOP ( 'NONE', ( #14296, #8223, #11137, #3368, #10794 ) ) ;
#13454=ORIENTED_EDGE ( 'NONE', *, *, #9935, .T. ) ;
#13458=DIRECTION ( 'NONE',  ( 0.000000000000000000, 0.000000000000000000, -1.000000000000000000 ) ) ;
#13470=EDGE_CURVE ( 'NONE', #4582, #3164, #8764, .T. ) ;
#13478=VECTOR ( 'NONE', #13672, 1000.000000000000000 ) ;
#13479=LINE ( 'NONE', #1497, #5312 ) ;
#13484=VECTOR ( 'NONE', #12552, 1000.000000000000000 ) ;
#13513=DIRECTION ( 'NONE',  ( 0.000000000000000000, -0.5000000000000012212, -0.8660254037844380415 ) ) ;
#13533=CARTESIAN_POINT ( 'NONE',  ( 2.500000000000000000, -1.178949249685213863, 2.042000000000002924 ) ) ;
#13535=AXIS2_PLACEMENT_3D ( 'NONE', #63, #9893, #1450 ) ;
#13550=AXIS2_PLACEMENT_3D ( 'NONE', #8767, #1943, #3267 ) ;
#13551=CARTESIAN_POINT ( 'NONE',  ( 2.500000000000000000, 2.357898499370433054, -1.951563910473907981E-15 ) ) ;
#13574=ORIENTED_EDGE ( 'NONE', *, *, #7635, .T. ) ;
#13589=DIRECTION ( 'NONE',  ( 1.000000000000000000, 0.000000000000000000, 0.000000000000000000 ) ) ;
#13609=EDGE_CURVE ( 'NONE', #3237, #13622, #7425, .T. ) ;
#13615=LINE ( 'NONE', #4857, #2939 ) ;
#13622=VERTEX_POINT ( 'NONE', #4240 ) ;
#13639=( LENGTH_UNIT ( ) NAMED_UNIT ( * ) SI_UNIT ( .MILLI., .METRE. ) );
#13645=ORIENTED_EDGE ( 'NONE', *, *, #12279, .T. ) ;
#13659=VECTOR ( 'NONE', #7590, 1000.000000000000000 ) ;
#13672=DIRECTION ( 'NONE',  ( -1.000000000000000000, -0.000000000000000000, -0.000000000000000000 ) ) ;
#13682=ORIENTED_EDGE ( 'NONE', *, *, #1880, .T. ) ;
#13688=PLANE ( 'NONE',  #3614 ) ;
#13695=CIRCLE ( 'NONE', #7452, 2.041999999999999815 ) ;
#13696=ORIENTED_EDGE ( 'NONE', *, *, #5751, .F. ) ;
#13784=SHAPE_REPRESENTATION_RELATIONSHIP ( 'NONE' , 'NONE' ,  #13104, #1425 ) ;
#13787=DIRECTION ( 'NONE',  ( 0.000000000000000000, 0.000000000000000000, -1.000000000000000000 ) ) ;
#13793=ORIENTED_EDGE ( 'NONE', *, *, #7468, .F. ) ;
#13823=AXIS2_PLACEMENT_3D ( 'NONE', #12278, #6972, #9147 ) ;
#13845=CARTESIAN_POINT ( 'NONE',  ( 2.500000000000000000, 1.178949249685213863, -2.042000000000001148 ) ) ;
#13918=ORIENTED_EDGE ( 'NONE', *, *, #1162, .F. ) ;
#13936=ORIENTED_EDGE ( 'NONE', *, *, #2410, .F. ) ;
#13957=COLOUR_RGB ( '',1.000000000000000000, 0.9490196078431372140, 0.9098039215686274384 ) ;
#13973=ORIENTED_EDGE ( 'NONE', *, *, #2005, .T. ) ;
#13974=DIRECTION ( 'NONE',  ( 0.000000000000000000, -1.287488025362403787E-15, -1.000000000000000000 ) ) ;
#14039=AXIS2_PLACEMENT_3D ( 'NONE', #10508, #9418, #5077 ) ;
#14089=CARTESIAN_POINT ( 'NONE',  ( 0.000000000000000000, -1.178949249685213863, 2.042000000000002924 ) ) ;
#14102=EDGE_CURVE ( 'NONE', #12266, #1400, #11080, .T. ) ;
#14116=DIRECTION ( 'NONE',  ( 0.000000000000000000, 0.000000000000000000, 1.000000000000000000 ) ) ;
#14128=DIRECTION ( 'NONE',  ( 0.000000000000000000, -1.000000000000000000, 1.287488025362403787E-15 ) ) ;
#14132=DIRECTION ( 'NONE',  ( 0.000000000000000000, -0.4999999999999993894, 0.8660254037844389297 ) ) ;
#14155=ORIENTED_EDGE ( 'NONE', *, *, #1843, .F. ) ;
#14179=CARTESIAN_POINT ( 'NONE',  ( 5.000000000000002665, 0.000000000000000000, -2.700000000000001066 ) ) ;
#14201=ORIENTED_EDGE ( 'NONE', *, *, #4395, .F. ) ;
#14218=DIRECTION ( 'NONE',  ( -1.000000000000000000, -0.000000000000000000, -0.000000000000000000 ) ) ;
#14239=ORIENTED_EDGE ( 'NONE', *, *, #1007, .F. ) ;
#14248=PLANE ( 'NONE',  #10075 ) ;
#14251=EDGE_CURVE ( 'NONE', #722, #1400, #7749, .T. ) ;
#14258=ADVANCED_FACE ( 'NONE', ( #3352 ), #8703, .F. ) ;
#14260=ADVANCED_FACE ( 'NONE', ( #42 ), #4501, .T. ) ;
#14279=AXIS2_PLACEMENT_3D ( 'NONE', #9996, #10200, #4702 ) ;
#14291=EDGE_CURVE ( 'NONE', #8299, #8193, #7025, .T. ) ;
#14296=ORIENTED_EDGE ( 'NONE', *, *, #7726, .F. ) ;
#14411=COLOUR_RGB('Black',0.12,0.14,0.17);
#14412=FILL_AREA_STYLE_COLOUR('',#14411);
#14413=FILL_AREA_STYLE('',(#14412));
#14414=SURFACE_STYLE_FILL_AREA(#14413);
#14415=SURFACE_SIDE_STYLE('',(#14414));
#14416=SURFACE_STYLE_USAGE(.BOTH.,#14415);
#14417=PRESENTATION_STYLE_ASSIGNMENT((#14416));
ENDSEC;
END-ISO-10303-21;
